ISO-10303-21;
HEADER;
/* Generated by software containing ST-Developer
 * from STEP Tools, Inc. (www.steptools.com) 
 */

FILE_DESCRIPTION(
/* description */ ('STEP AP214'),
/* implementation_level */ '2;1');

FILE_NAME(
/* name */ 'Socket Flat Head Screw M4x0.7x16.step',
/* time_stamp */ '2026-11-14T21:53:28-08:00',
/* author */ (''),
/* organization */ (''),
/* preprocessor_version */ 'ST-DEVELOPER v20.2',
/* originating_system */ 'Autodesk Translation Framework v15.17.0.0',
/* authorisation */ '');

FILE_SCHEMA (('AUTOMOTIVE_DESIGN { 1 0 10303 214 3 1 1 }'));
ENDSEC;

DATA;
#10=MECHANICAL_DESIGN_GEOMETRIC_PRESENTATION_REPRESENTATION('',(#352),#20176);
#220=CONICAL_SURFACE('',#12152,1.25,1.04719755119659);
#221=CONICAL_SURFACE('',#12166,3.9,0.785398163397451);
#222=CONICAL_SURFACE('',#12169,1.61,0.785398163397478);
#231=TOROIDAL_SURFACE('',#12159,2.2,0.2);
#305=SHAPE_REPRESENTATION_RELATIONSHIP('SRR','None',#20269,#317);
#317=ADVANCED_BREP_SHAPE_REPRESENTATION('',(#379),#20175);
#352=STYLED_ITEM('',(#20337),#379);
#379=MANIFOLD_SOLID_BREP('Body1',#10970);
#575=FACE_BOUND('',#2266,.T.);
#886=PLANE('',#12171);
#887=PLANE('',#12172);
#888=PLANE('',#12173);
#889=PLANE('',#12174);
#890=PLANE('',#12175);
#891=PLANE('',#12176);
#892=PLANE('',#12177);
#893=PLANE('',#12178);
#894=PLANE('',#12179);
#895=PLANE('',#12180);
#896=PLANE('',#12181);
#897=PLANE('',#12182);
#898=PLANE('',#12183);
#899=PLANE('',#12184);
#1472=FACE_OUTER_BOUND('',#2259,.T.);
#1473=FACE_OUTER_BOUND('',#2260,.T.);
#1474=FACE_OUTER_BOUND('',#2261,.T.);
#1475=FACE_OUTER_BOUND('',#2262,.T.);
#1476=FACE_OUTER_BOUND('',#2263,.T.);
#1477=FACE_OUTER_BOUND('',#2264,.T.);
#1478=FACE_OUTER_BOUND('',#2265,.T.);
#1479=FACE_OUTER_BOUND('',#2267,.T.);
#1480=FACE_OUTER_BOUND('',#2268,.T.);
#1481=FACE_OUTER_BOUND('',#2269,.T.);
#1482=FACE_OUTER_BOUND('',#2270,.T.);
#1483=FACE_OUTER_BOUND('',#2271,.T.);
#1484=FACE_OUTER_BOUND('',#2272,.T.);
#1485=FACE_OUTER_BOUND('',#2273,.T.);
#1486=FACE_OUTER_BOUND('',#2274,.T.);
#1487=FACE_OUTER_BOUND('',#2275,.T.);
#1488=FACE_OUTER_BOUND('',#2276,.T.);
#1489=FACE_OUTER_BOUND('',#2277,.T.);
#1490=FACE_OUTER_BOUND('',#2278,.T.);
#1491=FACE_OUTER_BOUND('',#2279,.T.);
#2259=EDGE_LOOP('',(#10061,#10062,#10063,#10064,#10065,#10066,#10067,#10068));
#2260=EDGE_LOOP('',(#10069,#10070,#10071,#10072));
#2261=EDGE_LOOP('',(#10073,#10074,#10075,#10076));
#2262=EDGE_LOOP('',(#10077,#10078,#10079,#10080));
#2263=EDGE_LOOP('',(#10081,#10082,#10083,#10084));
#2264=EDGE_LOOP('',(#10085,#10086,#10087,#10088));
#2265=EDGE_LOOP('',(#10089));
#2266=EDGE_LOOP('',(#10090,#10091,#10092,#10093,#10094,#10095));
#2267=EDGE_LOOP('',(#10096));
#2268=EDGE_LOOP('',(#10097,#10098,#10099,#10100,#10101));
#2269=EDGE_LOOP('',(#10102,#10103,#10104,#10105,#10106));
#2270=EDGE_LOOP('',(#10107,#10108,#10109,#10110,#10111));
#2271=EDGE_LOOP('',(#10112,#10113,#10114,#10115,#10116));
#2272=EDGE_LOOP('',(#10117,#10118,#10119,#10120,#10121));
#2273=EDGE_LOOP('',(#10122,#10123,#10124,#10125,#10126));
#2274=EDGE_LOOP('',(#10127,#10128,#10129));
#2275=EDGE_LOOP('',(#10130,#10131,#10132));
#2276=EDGE_LOOP('',(#10133,#10134,#10135));
#2277=EDGE_LOOP('',(#10136,#10137,#10138));
#2278=EDGE_LOOP('',(#10139,#10140,#10141));
#2279=EDGE_LOOP('',(#10142,#10143,#10144));
#3239=LINE('',#20032,#4227);
#3240=LINE('',#20054,#4228);
#3241=LINE('',#20057,#4229);
#3242=LINE('',#20060,#4230);
#3243=LINE('',#20064,#4231);
#3244=LINE('',#20069,#4232);
#3245=LINE('',#20071,#4233);
#3246=LINE('',#20073,#4234);
#3247=LINE('',#20075,#4235);
#3248=LINE('',#20077,#4236);
#3249=LINE('',#20078,#4237);
#3250=LINE('',#20082,#4238);
#3251=LINE('',#20083,#4239);
#3252=LINE('',#20085,#4240);
#3253=LINE('',#20086,#4241);
#3254=LINE('',#20088,#4242);
#3255=LINE('',#20090,#4243);
#3256=LINE('',#20091,#4244);
#3257=LINE('',#20093,#4245);
#3258=LINE('',#20095,#4246);
#3259=LINE('',#20096,#4247);
#3260=LINE('',#20098,#4248);
#3261=LINE('',#20100,#4249);
#3262=LINE('',#20101,#4250);
#3263=LINE('',#20103,#4251);
#3264=LINE('',#20105,#4252);
#3265=LINE('',#20106,#4253);
#3266=LINE('',#20108,#4254);
#3267=LINE('',#20109,#4255);
#4227=VECTOR('',#15271,1.25);
#4228=VECTOR('',#15296,3.9);
#4229=VECTOR('',#15301,3.9);
#4230=VECTOR('',#15304,2.);
#4231=VECTOR('',#15309,1.61);
#4232=VECTOR('',#15314,1000.);
#4233=VECTOR('',#15315,1000.);
#4234=VECTOR('',#15316,1000.);
#4235=VECTOR('',#15317,1000.);
#4236=VECTOR('',#15318,1000.);
#4237=VECTOR('',#15319,1000.);
#4238=VECTOR('',#15324,1000.);
#4239=VECTOR('',#15325,1000.);
#4240=VECTOR('',#15326,1000.);
#4241=VECTOR('',#15327,1000.);
#4242=VECTOR('',#15330,1000.);
#4243=VECTOR('',#15331,1000.);
#4244=VECTOR('',#15332,1000.);
#4245=VECTOR('',#15335,1000.);
#4246=VECTOR('',#15336,1000.);
#4247=VECTOR('',#15337,1000.);
#4248=VECTOR('',#15340,1000.);
#4249=VECTOR('',#15341,1000.);
#4250=VECTOR('',#15342,1000.);
#4251=VECTOR('',#15345,1000.);
#4252=VECTOR('',#15346,1000.);
#4253=VECTOR('',#15347,1000.);
#4254=VECTOR('',#15350,1000.);
#4255=VECTOR('',#15351,1000.);
#4714=CIRCLE('',#12153,1.25);
#4715=CIRCLE('',#12154,1.25);
#4716=CIRCLE('',#12155,1.25);
#4717=CIRCLE('',#12156,1.25);
#4718=CIRCLE('',#12157,1.25);
#4719=CIRCLE('',#12158,1.25);
#4720=CIRCLE('',#12160,2.05857864376269);
#4721=CIRCLE('',#12161,0.2);
#4722=CIRCLE('',#12162,2.);
#4723=CIRCLE('',#12164,3.9);
#4724=CIRCLE('',#12165,3.9);
#4725=CIRCLE('',#12168,2.);
#4726=CIRCLE('',#12170,1.61);
#5669=VERTEX_POINT('',#20030);
#5670=VERTEX_POINT('',#20031);
#5671=VERTEX_POINT('',#20033);
#5672=VERTEX_POINT('',#20035);
#5673=VERTEX_POINT('',#20037);
#5674=VERTEX_POINT('',#20039);
#5675=VERTEX_POINT('',#20041);
#5676=VERTEX_POINT('',#20045);
#5677=VERTEX_POINT('',#20047);
#5678=VERTEX_POINT('',#20051);
#5679=VERTEX_POINT('',#20053);
#5680=VERTEX_POINT('',#20059);
#5681=VERTEX_POINT('',#20063);
#5682=VERTEX_POINT('',#20067);
#5683=VERTEX_POINT('',#20068);
#5684=VERTEX_POINT('',#20070);
#5685=VERTEX_POINT('',#20072);
#5686=VERTEX_POINT('',#20074);
#5687=VERTEX_POINT('',#20076);
#5688=VERTEX_POINT('',#20081);
#5689=VERTEX_POINT('',#20084);
#5690=VERTEX_POINT('',#20089);
#5691=VERTEX_POINT('',#20094);
#5692=VERTEX_POINT('',#20099);
#5693=VERTEX_POINT('',#20104);
#7141=EDGE_CURVE('',#5669,#5670,#3239,.T.);
#7142=EDGE_CURVE('',#5670,#5671,#4714,.T.);
#7143=EDGE_CURVE('',#5671,#5672,#4715,.T.);
#7144=EDGE_CURVE('',#5672,#5673,#4716,.T.);
#7145=EDGE_CURVE('',#5673,#5674,#4717,.T.);
#7146=EDGE_CURVE('',#5674,#5675,#4718,.T.);
#7147=EDGE_CURVE('',#5675,#5670,#4719,.T.);
#7148=EDGE_CURVE('',#5676,#5676,#4720,.T.);
#7149=EDGE_CURVE('',#5676,#5677,#4721,.T.);
#7150=EDGE_CURVE('',#5677,#5677,#4722,.T.);
#7151=EDGE_CURVE('',#5678,#5678,#4723,.T.);
#7152=EDGE_CURVE('',#5678,#5679,#3240,.T.);
#7153=EDGE_CURVE('',#5679,#5679,#4724,.T.);
#7154=EDGE_CURVE('',#5679,#5676,#3241,.T.);
#7155=EDGE_CURVE('',#5677,#5680,#3242,.T.);
#7156=EDGE_CURVE('',#5680,#5680,#4725,.T.);
#7157=EDGE_CURVE('',#5680,#5681,#3243,.T.);
#7158=EDGE_CURVE('',#5681,#5681,#4726,.T.);
#7159=EDGE_CURVE('',#5682,#5683,#3244,.T.);
#7160=EDGE_CURVE('',#5683,#5684,#3245,.T.);
#7161=EDGE_CURVE('',#5684,#5685,#3246,.T.);
#7162=EDGE_CURVE('',#5685,#5686,#3247,.T.);
#7163=EDGE_CURVE('',#5686,#5687,#3248,.T.);
#7164=EDGE_CURVE('',#5687,#5682,#3249,.T.);
#7165=EDGE_CURVE('',#5688,#5683,#3250,.T.);
#7166=EDGE_CURVE('',#5688,#5671,#3251,.T.);
#7167=EDGE_CURVE('',#5671,#5689,#3252,.T.);
#7168=EDGE_CURVE('',#5689,#5684,#3253,.T.);
#7169=EDGE_CURVE('',#5689,#5670,#3254,.T.);
#7170=EDGE_CURVE('',#5670,#5690,#3255,.T.);
#7171=EDGE_CURVE('',#5690,#5685,#3256,.T.);
#7172=EDGE_CURVE('',#5690,#5675,#3257,.T.);
#7173=EDGE_CURVE('',#5675,#5691,#3258,.T.);
#7174=EDGE_CURVE('',#5691,#5686,#3259,.T.);
#7175=EDGE_CURVE('',#5691,#5674,#3260,.T.);
#7176=EDGE_CURVE('',#5674,#5692,#3261,.T.);
#7177=EDGE_CURVE('',#5692,#5687,#3262,.T.);
#7178=EDGE_CURVE('',#5692,#5673,#3263,.T.);
#7179=EDGE_CURVE('',#5673,#5693,#3264,.T.);
#7180=EDGE_CURVE('',#5693,#5682,#3265,.T.);
#7181=EDGE_CURVE('',#5693,#5672,#3266,.T.);
#7182=EDGE_CURVE('',#5672,#5688,#3267,.T.);
#10061=ORIENTED_EDGE('',*,*,#7141,.T.);
#10062=ORIENTED_EDGE('',*,*,#7142,.T.);
#10063=ORIENTED_EDGE('',*,*,#7143,.T.);
#10064=ORIENTED_EDGE('',*,*,#7144,.T.);
#10065=ORIENTED_EDGE('',*,*,#7145,.T.);
#10066=ORIENTED_EDGE('',*,*,#7146,.T.);
#10067=ORIENTED_EDGE('',*,*,#7147,.T.);
#10068=ORIENTED_EDGE('',*,*,#7141,.F.);
#10069=ORIENTED_EDGE('',*,*,#7148,.F.);
#10070=ORIENTED_EDGE('',*,*,#7149,.T.);
#10071=ORIENTED_EDGE('',*,*,#7150,.F.);
#10072=ORIENTED_EDGE('',*,*,#7149,.F.);
#10073=ORIENTED_EDGE('',*,*,#7151,.F.);
#10074=ORIENTED_EDGE('',*,*,#7152,.T.);
#10075=ORIENTED_EDGE('',*,*,#7153,.T.);
#10076=ORIENTED_EDGE('',*,*,#7152,.F.);
#10077=ORIENTED_EDGE('',*,*,#7153,.F.);
#10078=ORIENTED_EDGE('',*,*,#7154,.T.);
#10079=ORIENTED_EDGE('',*,*,#7148,.T.);
#10080=ORIENTED_EDGE('',*,*,#7154,.F.);
#10081=ORIENTED_EDGE('',*,*,#7150,.T.);
#10082=ORIENTED_EDGE('',*,*,#7155,.T.);
#10083=ORIENTED_EDGE('',*,*,#7156,.T.);
#10084=ORIENTED_EDGE('',*,*,#7155,.F.);
#10085=ORIENTED_EDGE('',*,*,#7156,.F.);
#10086=ORIENTED_EDGE('',*,*,#7157,.T.);
#10087=ORIENTED_EDGE('',*,*,#7158,.T.);
#10088=ORIENTED_EDGE('',*,*,#7157,.F.);
#10089=ORIENTED_EDGE('',*,*,#7151,.T.);
#10090=ORIENTED_EDGE('',*,*,#7159,.T.);
#10091=ORIENTED_EDGE('',*,*,#7160,.T.);
#10092=ORIENTED_EDGE('',*,*,#7161,.T.);
#10093=ORIENTED_EDGE('',*,*,#7162,.T.);
#10094=ORIENTED_EDGE('',*,*,#7163,.T.);
#10095=ORIENTED_EDGE('',*,*,#7164,.T.);
#10096=ORIENTED_EDGE('',*,*,#7158,.F.);
#10097=ORIENTED_EDGE('',*,*,#7160,.F.);
#10098=ORIENTED_EDGE('',*,*,#7165,.F.);
#10099=ORIENTED_EDGE('',*,*,#7166,.T.);
#10100=ORIENTED_EDGE('',*,*,#7167,.T.);
#10101=ORIENTED_EDGE('',*,*,#7168,.T.);
#10102=ORIENTED_EDGE('',*,*,#7161,.F.);
#10103=ORIENTED_EDGE('',*,*,#7168,.F.);
#10104=ORIENTED_EDGE('',*,*,#7169,.T.);
#10105=ORIENTED_EDGE('',*,*,#7170,.T.);
#10106=ORIENTED_EDGE('',*,*,#7171,.T.);
#10107=ORIENTED_EDGE('',*,*,#7162,.F.);
#10108=ORIENTED_EDGE('',*,*,#7171,.F.);
#10109=ORIENTED_EDGE('',*,*,#7172,.T.);
#10110=ORIENTED_EDGE('',*,*,#7173,.T.);
#10111=ORIENTED_EDGE('',*,*,#7174,.T.);
#10112=ORIENTED_EDGE('',*,*,#7163,.F.);
#10113=ORIENTED_EDGE('',*,*,#7174,.F.);
#10114=ORIENTED_EDGE('',*,*,#7175,.T.);
#10115=ORIENTED_EDGE('',*,*,#7176,.T.);
#10116=ORIENTED_EDGE('',*,*,#7177,.T.);
#10117=ORIENTED_EDGE('',*,*,#7164,.F.);
#10118=ORIENTED_EDGE('',*,*,#7177,.F.);
#10119=ORIENTED_EDGE('',*,*,#7178,.T.);
#10120=ORIENTED_EDGE('',*,*,#7179,.T.);
#10121=ORIENTED_EDGE('',*,*,#7180,.T.);
#10122=ORIENTED_EDGE('',*,*,#7159,.F.);
#10123=ORIENTED_EDGE('',*,*,#7180,.F.);
#10124=ORIENTED_EDGE('',*,*,#7181,.T.);
#10125=ORIENTED_EDGE('',*,*,#7182,.T.);
#10126=ORIENTED_EDGE('',*,*,#7165,.T.);
#10127=ORIENTED_EDGE('',*,*,#7144,.F.);
#10128=ORIENTED_EDGE('',*,*,#7181,.F.);
#10129=ORIENTED_EDGE('',*,*,#7179,.F.);
#10130=ORIENTED_EDGE('',*,*,#7143,.F.);
#10131=ORIENTED_EDGE('',*,*,#7166,.F.);
#10132=ORIENTED_EDGE('',*,*,#7182,.F.);
#10133=ORIENTED_EDGE('',*,*,#7142,.F.);
#10134=ORIENTED_EDGE('',*,*,#7169,.F.);
#10135=ORIENTED_EDGE('',*,*,#7167,.F.);
#10136=ORIENTED_EDGE('',*,*,#7147,.F.);
#10137=ORIENTED_EDGE('',*,*,#7172,.F.);
#10138=ORIENTED_EDGE('',*,*,#7170,.F.);
#10139=ORIENTED_EDGE('',*,*,#7146,.F.);
#10140=ORIENTED_EDGE('',*,*,#7175,.F.);
#10141=ORIENTED_EDGE('',*,*,#7173,.F.);
#10142=ORIENTED_EDGE('',*,*,#7145,.F.);
#10143=ORIENTED_EDGE('',*,*,#7178,.F.);
#10144=ORIENTED_EDGE('',*,*,#7176,.F.);
#10350=CYLINDRICAL_SURFACE('',#12163,3.9);
#10351=CYLINDRICAL_SURFACE('',#12167,2.);
#10924=ADVANCED_FACE('',(#1472),#220,.F.);
#10925=ADVANCED_FACE('',(#1473),#231,.F.);
#10926=ADVANCED_FACE('',(#1474),#10350,.T.);
#10927=ADVANCED_FACE('',(#1475),#221,.T.);
#10928=ADVANCED_FACE('',(#1476),#10351,.T.);
#10929=ADVANCED_FACE('',(#1477),#222,.T.);
#10930=ADVANCED_FACE('',(#1478,#575),#886,.T.);
#10931=ADVANCED_FACE('',(#1479),#887,.T.);
#10932=ADVANCED_FACE('',(#1480),#888,.T.);
#10933=ADVANCED_FACE('',(#1481),#889,.T.);
#10934=ADVANCED_FACE('',(#1482),#890,.T.);
#10935=ADVANCED_FACE('',(#1483),#891,.T.);
#10936=ADVANCED_FACE('',(#1484),#892,.T.);
#10937=ADVANCED_FACE('',(#1485),#893,.T.);
#10938=ADVANCED_FACE('',(#1486),#894,.T.);
#10939=ADVANCED_FACE('',(#1487),#895,.T.);
#10940=ADVANCED_FACE('',(#1488),#896,.T.);
#10941=ADVANCED_FACE('',(#1489),#897,.T.);
#10942=ADVANCED_FACE('',(#1490),#898,.T.);
#10943=ADVANCED_FACE('',(#1491),#899,.T.);
#10970=CLOSED_SHELL('',(#10924,#10925,#10926,#10927,#10928,#10929,#10930,
#10931,#10932,#10933,#10934,#10935,#10936,#10937,#10938,#10939,#10940,#10941,
#10942,#10943));
#12151=AXIS2_PLACEMENT_3D('',#20028,#15267,#15268);
#12152=AXIS2_PLACEMENT_3D('',#20029,#15269,#15270);
#12153=AXIS2_PLACEMENT_3D('',#20034,#15272,#15273);
#12154=AXIS2_PLACEMENT_3D('',#20036,#15274,#15275);
#12155=AXIS2_PLACEMENT_3D('',#20038,#15276,#15277);
#12156=AXIS2_PLACEMENT_3D('',#20040,#15278,#15279);
#12157=AXIS2_PLACEMENT_3D('',#20042,#15280,#15281);
#12158=AXIS2_PLACEMENT_3D('',#20043,#15282,#15283);
#12159=AXIS2_PLACEMENT_3D('',#20044,#15284,#15285);
#12160=AXIS2_PLACEMENT_3D('',#20046,#15286,#15287);
#12161=AXIS2_PLACEMENT_3D('',#20048,#15288,#15289);
#12162=AXIS2_PLACEMENT_3D('',#20049,#15290,#15291);
#12163=AXIS2_PLACEMENT_3D('',#20050,#15292,#15293);
#12164=AXIS2_PLACEMENT_3D('',#20052,#15294,#15295);
#12165=AXIS2_PLACEMENT_3D('',#20055,#15297,#15298);
#12166=AXIS2_PLACEMENT_3D('',#20056,#15299,#15300);
#12167=AXIS2_PLACEMENT_3D('',#20058,#15302,#15303);
#12168=AXIS2_PLACEMENT_3D('',#20061,#15305,#15306);
#12169=AXIS2_PLACEMENT_3D('',#20062,#15307,#15308);
#12170=AXIS2_PLACEMENT_3D('',#20065,#15310,#15311);
#12171=AXIS2_PLACEMENT_3D('',#20066,#15312,#15313);
#12172=AXIS2_PLACEMENT_3D('',#20079,#15320,#15321);
#12173=AXIS2_PLACEMENT_3D('',#20080,#15322,#15323);
#12174=AXIS2_PLACEMENT_3D('',#20087,#15328,#15329);
#12175=AXIS2_PLACEMENT_3D('',#20092,#15333,#15334);
#12176=AXIS2_PLACEMENT_3D('',#20097,#15338,#15339);
#12177=AXIS2_PLACEMENT_3D('',#20102,#15343,#15344);
#12178=AXIS2_PLACEMENT_3D('',#20107,#15348,#15349);
#12179=AXIS2_PLACEMENT_3D('',#20110,#15352,#15353);
#12180=AXIS2_PLACEMENT_3D('',#20111,#15354,#15355);
#12181=AXIS2_PLACEMENT_3D('',#20112,#15356,#15357);
#12182=AXIS2_PLACEMENT_3D('',#20113,#15358,#15359);
#12183=AXIS2_PLACEMENT_3D('',#20114,#15360,#15361);
#12184=AXIS2_PLACEMENT_3D('',#20115,#15362,#15363);
#15267=DIRECTION('axis',(0.,0.,1.));
#15268=DIRECTION('refdir',(1.,0.,0.));
#15269=DIRECTION('center_axis',(-1.,0.,0.));
#15270=DIRECTION('ref_axis',(0.,0.,1.));
#15271=DIRECTION('',(-0.500000000000004,-1.0605752387249E-16,-0.866025403784436));
#15272=DIRECTION('center_axis',(-1.,0.,0.));
#15273=DIRECTION('ref_axis',(0.,0.,1.));
#15274=DIRECTION('center_axis',(-1.,0.,0.));
#15275=DIRECTION('ref_axis',(0.,0.,1.));
#15276=DIRECTION('center_axis',(-1.,0.,0.));
#15277=DIRECTION('ref_axis',(0.,0.,1.));
#15278=DIRECTION('center_axis',(-1.,0.,0.));
#15279=DIRECTION('ref_axis',(0.,0.,1.));
#15280=DIRECTION('center_axis',(-1.,0.,0.));
#15281=DIRECTION('ref_axis',(0.,0.,1.));
#15282=DIRECTION('center_axis',(-1.,0.,0.));
#15283=DIRECTION('ref_axis',(0.,0.,1.));
#15284=DIRECTION('center_axis',(-1.,0.,0.));
#15285=DIRECTION('ref_axis',(0.,0.,1.));
#15286=DIRECTION('center_axis',(-1.,0.,0.));
#15287=DIRECTION('ref_axis',(0.,0.,1.));
#15288=DIRECTION('center_axis',(0.,1.,-1.22464679914735E-16));
#15289=DIRECTION('ref_axis',(0.,-1.22464679914735E-16,-1.));
#15290=DIRECTION('center_axis',(1.,0.,0.));
#15291=DIRECTION('ref_axis',(0.,0.,1.));
#15292=DIRECTION('center_axis',(-1.,0.,0.));
#15293=DIRECTION('ref_axis',(0.,0.,1.));
#15294=DIRECTION('center_axis',(-1.,0.,0.));
#15295=DIRECTION('ref_axis',(0.,0.,1.));
#15296=DIRECTION('',(1.,0.,0.));
#15297=DIRECTION('center_axis',(-1.,0.,0.));
#15298=DIRECTION('ref_axis',(0.,0.,1.));
#15299=DIRECTION('center_axis',(-1.,0.,0.));
#15300=DIRECTION('ref_axis',(0.,0.,1.));
#15301=DIRECTION('',(0.707106781186546,8.65956056235496E-17,0.70710678118655));
#15302=DIRECTION('center_axis',(-1.,0.,0.));
#15303=DIRECTION('ref_axis',(0.,0.,1.));
#15304=DIRECTION('',(1.,0.,0.));
#15305=DIRECTION('center_axis',(-1.,0.,0.));
#15306=DIRECTION('ref_axis',(0.,0.,1.));
#15307=DIRECTION('center_axis',(-1.,0.,0.));
#15308=DIRECTION('ref_axis',(0.,0.,1.));
#15309=DIRECTION('',(0.707106781186526,8.65956056235519E-17,0.707106781186569));
#15310=DIRECTION('center_axis',(-1.,0.,0.));
#15311=DIRECTION('ref_axis',(0.,0.,1.));
#15312=DIRECTION('center_axis',(-1.,0.,0.));
#15313=DIRECTION('ref_axis',(0.,0.,1.));
#15314=DIRECTION('',(0.,-0.500000000000001,-0.866025403784438));
#15315=DIRECTION('',(0.,0.5,-0.866025403784438));
#15316=DIRECTION('',(0.,1.,6.00925839494864E-16));
#15317=DIRECTION('',(0.,0.5,0.866025403784438));
#15318=DIRECTION('',(0.,-0.5,0.866025403784438));
#15319=DIRECTION('',(0.,-1.,0.));
#15320=DIRECTION('center_axis',(1.,0.,0.));
#15321=DIRECTION('ref_axis',(0.,0.,-1.));
#15322=DIRECTION('center_axis',(0.,0.866025403784438,0.500000000000001));
#15323=DIRECTION('ref_axis',(0.,-0.500000000000001,0.866025403784438));
#15324=DIRECTION('',(-1.,0.,0.));
#15325=DIRECTION('',(0.,0.5,-0.866025403784438));
#15326=DIRECTION('',(0.,0.5,-0.866025403784438));
#15327=DIRECTION('',(-1.,0.,0.));
#15328=DIRECTION('center_axis',(0.,-6.00925839494864E-16,1.));
#15329=DIRECTION('ref_axis',(0.,-1.,-6.00925839494864E-16));
#15330=DIRECTION('',(0.,1.,6.00925839494864E-16));
#15331=DIRECTION('',(0.,1.,6.00925839494864E-16));
#15332=DIRECTION('',(-1.,0.,0.));
#15333=DIRECTION('center_axis',(0.,-0.866025403784438,0.500000000000001));
#15334=DIRECTION('ref_axis',(0.,-0.500000000000001,-0.866025403784438));
#15335=DIRECTION('',(0.,0.5,0.866025403784438));
#15336=DIRECTION('',(0.,0.5,0.866025403784438));
#15337=DIRECTION('',(-1.,0.,0.));
#15338=DIRECTION('center_axis',(0.,-0.866025403784438,-0.5));
#15339=DIRECTION('ref_axis',(0.,0.5,-0.866025403784438));
#15340=DIRECTION('',(0.,-0.5,0.866025403784438));
#15341=DIRECTION('',(0.,-0.5,0.866025403784438));
#15342=DIRECTION('',(-1.,0.,0.));
#15343=DIRECTION('center_axis',(0.,0.,-1.));
#15344=DIRECTION('ref_axis',(-1.,0.,0.));
#15345=DIRECTION('',(0.,-1.,0.));
#15346=DIRECTION('',(0.,-1.,0.));
#15347=DIRECTION('',(-1.,0.,0.));
#15348=DIRECTION('center_axis',(0.,0.866025403784438,-0.500000000000001));
#15349=DIRECTION('ref_axis',(0.,0.500000000000001,0.866025403784438));
#15350=DIRECTION('',(0.,-0.500000000000001,-0.866025403784438));
#15351=DIRECTION('',(0.,-0.500000000000001,-0.866025403784438));
#15352=DIRECTION('center_axis',(-1.,0.,0.));
#15353=DIRECTION('ref_axis',(0.,0.,1.));
#15354=DIRECTION('center_axis',(-1.,0.,0.));
#15355=DIRECTION('ref_axis',(0.,0.,1.));
#15356=DIRECTION('center_axis',(-1.,0.,0.));
#15357=DIRECTION('ref_axis',(0.,0.,1.));
#15358=DIRECTION('center_axis',(-1.,0.,0.));
#15359=DIRECTION('ref_axis',(0.,0.,1.));
#15360=DIRECTION('center_axis',(-1.,0.,0.));
#15361=DIRECTION('ref_axis',(0.,0.,1.));
#15362=DIRECTION('center_axis',(-1.,0.,0.));
#15363=DIRECTION('ref_axis',(0.,0.,1.));
#20028=CARTESIAN_POINT('',(0.,0.,0.));
#20029=CARTESIAN_POINT('Origin',(1.5,0.,0.));
#20030=CARTESIAN_POINT('',(2.22168783648704,-1.82728999845763E-16,0.));
#20031=CARTESIAN_POINT('',(1.5,7.5115729936858E-16,-1.25));
#20032=CARTESIAN_POINT('',(1.5,-1.53080849893419E-16,-1.25));
#20033=CARTESIAN_POINT('',(1.5,-1.08253175473055,-0.625000000000001));
#20034=CARTESIAN_POINT('Origin',(1.5,0.,0.));
#20035=CARTESIAN_POINT('',(1.5,-1.08253175473055,0.625000000000002));
#20036=CARTESIAN_POINT('Origin',(1.5,0.,0.));
#20037=CARTESIAN_POINT('',(1.5,0.,1.25));
#20038=CARTESIAN_POINT('Origin',(1.5,0.,0.));
#20039=CARTESIAN_POINT('',(1.5,1.08253175473055,0.625));
#20040=CARTESIAN_POINT('Origin',(1.5,0.,0.));
#20041=CARTESIAN_POINT('',(1.5,1.08253175473055,-0.625000000000001));
#20042=CARTESIAN_POINT('Origin',(1.5,0.,0.));
#20043=CARTESIAN_POINT('Origin',(1.5,0.,0.));
#20044=CARTESIAN_POINT('Origin',(2.56284271247462,0.,0.));
#20045=CARTESIAN_POINT('',(2.42142135623731,-2.52103174687708E-16,-2.05857864376269));
#20046=CARTESIAN_POINT('Origin',(2.42142135623731,0.,0.));
#20047=CARTESIAN_POINT('',(2.56284271247462,-2.4492935982947E-16,-2.));
#20048=CARTESIAN_POINT('Origin',(2.56284271247462,-2.69422295812418E-16,
-2.2));
#20049=CARTESIAN_POINT('Origin',(2.56284271247462,0.,0.));
#20050=CARTESIAN_POINT('Origin',(0.,0.,0.));
#20051=CARTESIAN_POINT('',(0.,-4.77612251667468E-16,-3.9));
#20052=CARTESIAN_POINT('Origin',(0.,0.,0.));
#20053=CARTESIAN_POINT('',(0.580000000000009,-4.77612251667468E-16,-3.9));
#20054=CARTESIAN_POINT('',(0.,-4.77612251667468E-16,-3.9));
#20055=CARTESIAN_POINT('Origin',(0.580000000000009,0.,0.));
#20056=CARTESIAN_POINT('Origin',(0.580000000000009,0.,0.));
#20057=CARTESIAN_POINT('',(0.580000000000009,-4.77612251667468E-16,-3.9));
#20058=CARTESIAN_POINT('Origin',(0.,0.,0.));
#20059=CARTESIAN_POINT('',(15.61,-2.4492935982947E-16,-2.));
#20060=CARTESIAN_POINT('',(0.,-2.4492935982947E-16,-2.));
#20061=CARTESIAN_POINT('Origin',(15.61,0.,0.));
#20062=CARTESIAN_POINT('Origin',(16.,0.,0.));
#20063=CARTESIAN_POINT('',(16.,-1.97168134662724E-16,-1.61));
#20064=CARTESIAN_POINT('',(16.,-1.97168134662724E-16,-1.61));
#20065=CARTESIAN_POINT('Origin',(16.,0.,0.));
#20066=CARTESIAN_POINT('Origin',(0.,0.,0.));
#20067=CARTESIAN_POINT('',(0.,-0.721687836487031,1.25));
#20068=CARTESIAN_POINT('',(0.,-1.44337567297407,3.25260651745651E-16));
#20069=CARTESIAN_POINT('',(0.,-0.721687836487031,1.25));
#20070=CARTESIAN_POINT('',(0.,-0.721687836487032,-1.25));
#20071=CARTESIAN_POINT('',(0.,-1.44337567297407,3.72758124193626E-16));
#20072=CARTESIAN_POINT('',(0.,0.721687836487033,-1.25));
#20073=CARTESIAN_POINT('',(0.,-0.721687836487032,-1.25));
#20074=CARTESIAN_POINT('',(0.,1.44337567297407,-3.23360327335785E-17));
#20075=CARTESIAN_POINT('',(0.,0.721687836487033,-1.25));
#20076=CARTESIAN_POINT('',(0.,0.721687836487033,1.25));
#20077=CARTESIAN_POINT('',(0.,1.44337567297407,-3.23360327335785E-17));
#20078=CARTESIAN_POINT('',(0.,0.721687836487033,1.25));
#20079=CARTESIAN_POINT('Origin',(16.,1.61,0.));
#20080=CARTESIAN_POINT('Origin',(1.5,-1.44337567297407,3.72758124193626E-16));
#20081=CARTESIAN_POINT('',(1.5,-1.44337567297407,3.72758124193626E-16));
#20082=CARTESIAN_POINT('',(1.5,-1.44337567297407,3.72758124193626E-16));
#20083=CARTESIAN_POINT('',(1.5,-1.44337567297407,3.72758124193626E-16));
#20084=CARTESIAN_POINT('',(1.5,-0.721687836487032,-1.25));
#20085=CARTESIAN_POINT('',(1.5,-1.44337567297407,3.72758124193626E-16));
#20086=CARTESIAN_POINT('',(1.5,-0.721687836487032,-1.25));
#20087=CARTESIAN_POINT('Origin',(1.5,-0.721687836487032,-1.25));
#20088=CARTESIAN_POINT('',(1.5,-0.721687836487032,-1.25));
#20089=CARTESIAN_POINT('',(1.5,0.721687836487033,-1.25));
#20090=CARTESIAN_POINT('',(1.5,-0.721687836487032,-1.25));
#20091=CARTESIAN_POINT('',(1.5,0.721687836487033,-1.25));
#20092=CARTESIAN_POINT('Origin',(1.5,0.721687836487033,-1.25));
#20093=CARTESIAN_POINT('',(1.5,0.721687836487033,-1.25));
#20094=CARTESIAN_POINT('',(1.5,1.44337567297407,-3.23360327335785E-17));
#20095=CARTESIAN_POINT('',(1.5,0.721687836487033,-1.25));
#20096=CARTESIAN_POINT('',(1.5,1.44337567297407,-3.23360327335785E-17));
#20097=CARTESIAN_POINT('Origin',(1.5,1.44337567297407,-3.23360327335785E-17));
#20098=CARTESIAN_POINT('',(1.5,1.44337567297407,-3.23360327335785E-17));
#20099=CARTESIAN_POINT('',(1.5,0.721687836487033,1.25));
#20100=CARTESIAN_POINT('',(1.5,1.44337567297407,-3.23360327335785E-17));
#20101=CARTESIAN_POINT('',(1.5,0.721687836487033,1.25));
#20102=CARTESIAN_POINT('Origin',(1.5,0.721687836487033,1.25));
#20103=CARTESIAN_POINT('',(1.5,0.721687836487033,1.25));
#20104=CARTESIAN_POINT('',(1.5,-0.721687836487031,1.25));
#20105=CARTESIAN_POINT('',(1.5,0.721687836487033,1.25));
#20106=CARTESIAN_POINT('',(1.5,-0.721687836487031,1.25));
#20107=CARTESIAN_POINT('Origin',(1.5,-0.721687836487031,1.25));
#20108=CARTESIAN_POINT('',(1.5,-0.721687836487031,1.25));
#20109=CARTESIAN_POINT('',(1.5,-0.721687836487031,1.25));
#20110=CARTESIAN_POINT('Origin',(1.5,-1.44337567297407,4.33680868994202E-16));
#20111=CARTESIAN_POINT('Origin',(1.5,-1.44337567297407,4.33680868994202E-16));
#20112=CARTESIAN_POINT('Origin',(1.5,-1.44337567297407,4.33680868994202E-16));
#20113=CARTESIAN_POINT('Origin',(1.5,-1.44337567297407,4.33680868994202E-16));
#20114=CARTESIAN_POINT('Origin',(1.5,-1.44337567297407,4.33680868994202E-16));
#20115=CARTESIAN_POINT('Origin',(1.5,-1.44337567297407,4.33680868994202E-16));
#20159=UNCERTAINTY_MEASURE_WITH_UNIT(LENGTH_MEASURE(0.01),#20177,
'DISTANCE_ACCURACY_VALUE',
'Maximum model space distance between geometric entities at asserted c
onnectivities');
#20160=UNCERTAINTY_MEASURE_WITH_UNIT(LENGTH_MEASURE(0.01),#20177,
'DISTANCE_ACCURACY_VALUE',
'Maximum model space distance between geometric entities at asserted c
onnectivities');
#20175=(
GEOMETRIC_REPRESENTATION_CONTEXT(3)
GLOBAL_UNCERTAINTY_ASSIGNED_CONTEXT((#20159))
GLOBAL_UNIT_ASSIGNED_CONTEXT((#20177,#20179,#20180))
REPRESENTATION_CONTEXT('','3D')
);
#20176=(
GEOMETRIC_REPRESENTATION_CONTEXT(3)
GLOBAL_UNCERTAINTY_ASSIGNED_CONTEXT((#20160))
GLOBAL_UNIT_ASSIGNED_CONTEXT((#20177,#20179,#20180))
REPRESENTATION_CONTEXT('','3D')
);
#20177=(
LENGTH_UNIT()
NAMED_UNIT(*)
SI_UNIT(.MILLI.,.METRE.)
);
#20179=(
NAMED_UNIT(*)
PLANE_ANGLE_UNIT()
SI_UNIT($,.RADIAN.)
);
#20180=(
NAMED_UNIT(*)
SI_UNIT($,.STERADIAN.)
SOLID_ANGLE_UNIT()
);
#20195=SHAPE_DEFINITION_REPRESENTATION(#20225,#20269);
#20225=PRODUCT_DEFINITION_SHAPE('',$,#20285);
#20269=SHAPE_REPRESENTATION('',(#12151),#20175);
#20270=PRODUCT_DEFINITION_CONTEXT('part definition',#20317,'design');
#20285=PRODUCT_DEFINITION('Socket Flat Head Screw M4x0.7x16',
'Socket Flat Head Screw M4x0.7x16',#20300,#20270);
#20300=PRODUCT_DEFINITION_FORMATION('',$,#20333);
#20317=APPLICATION_CONTEXT(
'Core Data for Automotive Mechanical Design Process');
#20318=PRODUCT_CONTEXT('part definition',#20317,'mechanical');
#20333=PRODUCT('Socket Flat Head Screw M4x0.7x16',
'Socket Flat Head Screw M4x0.7x16',$,(#20318));
#20337=PRESENTATION_STYLE_ASSIGNMENT((#20342));
#20342=SURFACE_STYLE_USAGE(.BOTH.,#20347);
#20347=SURFACE_SIDE_STYLE('',(#20352));
#20352=SURFACE_STYLE_FILL_AREA(#20357);
#20357=FILL_AREA_STYLE('Opaque(31,36,43)',(#20362));
#20362=FILL_AREA_STYLE_COLOUR('Opaque(31,36,43)',#20367);
#20367=COLOUR_RGB('Opaque(31,36,43)',0.12156862745098,0.141176470588235,
0.168627450980392);
ENDSEC;
END-ISO-10303-21;
